ISO-10303-21;
HEADER;
/* Generated by software containing ST-Developer
 * from STEP Tools, Inc. (www.steptools.com) 
 */

FILE_DESCRIPTION(
/* description */ (''),
/* implementation_level */ '2;1');

FILE_NAME(
/* name */ 'Broached Hexagon Socket Head Cap Screw ASME B18.3.1M - M6x1 x 16 Stee_l Grade 2 Plain v1.step',
/* time_stamp */ '2026-10-12T15:29:24-07:00',
/* author */ (''),
/* organization */ (''),
/* preprocessor_version */ 'ST-DEVELOPER v20.2',
/* originating_system */ 'Autodesk Translation Framework v15.15.0.0',
/* authorisation */ '');

FILE_SCHEMA (('AUTOMOTIVE_DESIGN { 1 0 10303 214 3 1 1 }'));
ENDSEC;

DATA;
#10=MECHANICAL_DESIGN_GEOMETRIC_PRESENTATION_REPRESENTATION('',(#194),#9496);
#115=CONICAL_SURFACE('',#5516,2.72327499999996,0.831988093682975);
#130=TOROIDAL_SURFACE('',#5519,4.39999999999977,0.6);
#148=SHAPE_REPRESENTATION_RELATIONSHIP('SRR','None',#9542,#157);
#157=ADVANCED_BREP_SHAPE_REPRESENTATION('',(#251),#9490);
#194=STYLED_ITEM('',(#9594),#251);
#251=MANIFOLD_SOLID_BREP('Body1',#4996);
#412=FACE_BOUND('',#1219,.T.);
#413=FACE_BOUND('',#1236,.T.);
#545=PLANE('',#5523);
#546=PLANE('',#5526);
#547=PLANE('',#5527);
#548=PLANE('',#5528);
#549=PLANE('',#5529);
#550=PLANE('',#5530);
#551=PLANE('',#5531);
#552=PLANE('',#5532);
#553=PLANE('',#5533);
#554=PLANE('',#5534);
#555=PLANE('',#5535);
#556=PLANE('',#5536);
#557=PLANE('',#5537);
#558=PLANE('',#5540);
#559=PLANE('',#5541);
#805=FACE_OUTER_BOUND('',#1216,.T.);
#806=FACE_OUTER_BOUND('',#1217,.T.);
#807=FACE_OUTER_BOUND('',#1218,.T.);
#808=FACE_OUTER_BOUND('',#1220,.T.);
#809=FACE_OUTER_BOUND('',#1221,.T.);
#810=FACE_OUTER_BOUND('',#1222,.T.);
#811=FACE_OUTER_BOUND('',#1223,.T.);
#812=FACE_OUTER_BOUND('',#1224,.T.);
#813=FACE_OUTER_BOUND('',#1225,.T.);
#814=FACE_OUTER_BOUND('',#1226,.T.);
#815=FACE_OUTER_BOUND('',#1227,.T.);
#816=FACE_OUTER_BOUND('',#1228,.T.);
#817=FACE_OUTER_BOUND('',#1229,.T.);
#818=FACE_OUTER_BOUND('',#1230,.T.);
#819=FACE_OUTER_BOUND('',#1231,.T.);
#820=FACE_OUTER_BOUND('',#1232,.T.);
#821=FACE_OUTER_BOUND('',#1233,.T.);
#822=FACE_OUTER_BOUND('',#1234,.T.);
#823=FACE_OUTER_BOUND('',#1235,.T.);
#1216=EDGE_LOOP('',(#3961,#3962,#3963,#3964));
#1217=EDGE_LOOP('',(#3965,#3966,#3967,#3968));
#1218=EDGE_LOOP('',(#3969));
#1219=EDGE_LOOP('',(#3970,#3971,#3972,#3973,#3974,#3975));
#1220=EDGE_LOOP('',(#3976,#3977,#3978,#3979));
#1221=EDGE_LOOP('',(#3980,#3981,#3982));
#1222=EDGE_LOOP('',(#3983,#3984,#3985));
#1223=EDGE_LOOP('',(#3986,#3987,#3988));
#1224=EDGE_LOOP('',(#3989,#3990,#3991));
#1225=EDGE_LOOP('',(#3992,#3993,#3994));
#1226=EDGE_LOOP('',(#3995,#3996,#3997));
#1227=EDGE_LOOP('',(#3998,#3999,#4000,#4001));
#1228=EDGE_LOOP('',(#4002,#4003,#4004,#4005));
#1229=EDGE_LOOP('',(#4006,#4007,#4008,#4009));
#1230=EDGE_LOOP('',(#4010,#4011,#4012,#4013));
#1231=EDGE_LOOP('',(#4014,#4015,#4016,#4017));
#1232=EDGE_LOOP('',(#4018,#4019,#4020,#4021));
#1233=EDGE_LOOP('',(#4022,#4023,#4024,#4025));
#1234=EDGE_LOOP('',(#4026));
#1235=EDGE_LOOP('',(#4027));
#1236=EDGE_LOOP('',(#4028));
#1535=LINE('',#8527,#1772);
#1536=LINE('',#8538,#1773);
#1537=LINE('',#8540,#1774);
#1538=LINE('',#8542,#1775);
#1539=LINE('',#8544,#1776);
#1540=LINE('',#8546,#1777);
#1541=LINE('',#8547,#1778);
#1542=LINE('',#8551,#1779);
#1543=LINE('',#8555,#1780);
#1544=LINE('',#8557,#1781);
#1545=LINE('',#8558,#1782);
#1546=LINE('',#8561,#1783);
#1547=LINE('',#8562,#1784);
#1548=LINE('',#8565,#1785);
#1549=LINE('',#8566,#1786);
#1550=LINE('',#8569,#1787);
#1551=LINE('',#8570,#1788);
#1552=LINE('',#8573,#1789);
#1553=LINE('',#8574,#1790);
#1554=LINE('',#8576,#1791);
#1555=LINE('',#8578,#1792);
#1556=LINE('',#8579,#1793);
#1557=LINE('',#8581,#1794);
#1558=LINE('',#8583,#1795);
#1559=LINE('',#8585,#1796);
#1560=LINE('',#8587,#1797);
#1561=LINE('',#8591,#1798);
#1772=VECTOR('',#6718,2.72327499999996);
#1773=VECTOR('',#6731,10.);
#1774=VECTOR('',#6732,10.);
#1775=VECTOR('',#6733,10.);
#1776=VECTOR('',#6734,10.);
#1777=VECTOR('',#6735,9.99999999999999);
#1778=VECTOR('',#6736,10.);
#1779=VECTOR('',#6741,4.99999999999977);
#1780=VECTOR('',#6744,9.99999999999999);
#1781=VECTOR('',#6745,10.);
#1782=VECTOR('',#6746,10.);
#1783=VECTOR('',#6749,10.);
#1784=VECTOR('',#6750,10.);
#1785=VECTOR('',#6753,9.99999999999999);
#1786=VECTOR('',#6754,9.99999999999999);
#1787=VECTOR('',#6757,10.);
#1788=VECTOR('',#6758,10.);
#1789=VECTOR('',#6761,10.);
#1790=VECTOR('',#6762,10.);
#1791=VECTOR('',#6765,10.);
#1792=VECTOR('',#6768,10.);
#1793=VECTOR('',#6769,10.);
#1794=VECTOR('',#6772,10.);
#1795=VECTOR('',#6775,10.);
#1796=VECTOR('',#6778,10.);
#1797=VECTOR('',#6781,10.);
#1798=VECTOR('',#6786,2.942);
#2125=CIRCLE('',#5517,2.942);
#2126=CIRCLE('',#5518,2.38654999999999);
#2127=CIRCLE('',#5520,4.99999999999977);
#2128=CIRCLE('',#5521,0.6);
#2129=CIRCLE('',#5522,4.39999999999977);
#2130=CIRCLE('',#5525,4.99999999999977);
#2131=CIRCLE('',#5539,2.942);
#2498=VERTEX_POINT('',#8524);
#2499=VERTEX_POINT('',#8526);
#2500=VERTEX_POINT('',#8530);
#2501=VERTEX_POINT('',#8532);
#2502=VERTEX_POINT('',#8536);
#2503=VERTEX_POINT('',#8537);
#2504=VERTEX_POINT('',#8539);
#2505=VERTEX_POINT('',#8541);
#2506=VERTEX_POINT('',#8543);
#2507=VERTEX_POINT('',#8545);
#2508=VERTEX_POINT('',#8549);
#2509=VERTEX_POINT('',#8553);
#2510=VERTEX_POINT('',#8554);
#2511=VERTEX_POINT('',#8556);
#2512=VERTEX_POINT('',#8560);
#2513=VERTEX_POINT('',#8564);
#2514=VERTEX_POINT('',#8568);
#2515=VERTEX_POINT('',#8572);
#2516=VERTEX_POINT('',#8590);
#3033=EDGE_CURVE('',#2498,#2498,#2125,.T.);
#3034=EDGE_CURVE('',#2498,#2499,#1535,.T.);
#3035=EDGE_CURVE('',#2499,#2499,#2126,.T.);
#3036=EDGE_CURVE('',#2500,#2500,#2127,.T.);
#3037=EDGE_CURVE('',#2500,#2501,#2128,.T.);
#3038=EDGE_CURVE('',#2501,#2501,#2129,.T.);
#3039=EDGE_CURVE('',#2502,#2503,#1536,.T.);
#3040=EDGE_CURVE('',#2503,#2504,#1537,.T.);
#3041=EDGE_CURVE('',#2504,#2505,#1538,.T.);
#3042=EDGE_CURVE('',#2505,#2506,#1539,.T.);
#3043=EDGE_CURVE('',#2506,#2507,#1540,.T.);
#3044=EDGE_CURVE('',#2507,#2502,#1541,.T.);
#3045=EDGE_CURVE('',#2508,#2508,#2130,.T.);
#3046=EDGE_CURVE('',#2508,#2500,#1542,.T.);
#3047=EDGE_CURVE('',#2509,#2510,#1543,.T.);
#3048=EDGE_CURVE('',#2511,#2509,#1544,.T.);
#3049=EDGE_CURVE('',#2511,#2510,#1545,.T.);
#3050=EDGE_CURVE('',#2512,#2511,#1546,.T.);
#3051=EDGE_CURVE('',#2512,#2510,#1547,.T.);
#3052=EDGE_CURVE('',#2513,#2512,#1548,.T.);
#3053=EDGE_CURVE('',#2513,#2510,#1549,.T.);
#3054=EDGE_CURVE('',#2514,#2513,#1550,.T.);
#3055=EDGE_CURVE('',#2514,#2510,#1551,.T.);
#3056=EDGE_CURVE('',#2515,#2514,#1552,.T.);
#3057=EDGE_CURVE('',#2515,#2510,#1553,.T.);
#3058=EDGE_CURVE('',#2509,#2515,#1554,.T.);
#3059=EDGE_CURVE('',#2502,#2511,#1555,.T.);
#3060=EDGE_CURVE('',#2503,#2509,#1556,.T.);
#3061=EDGE_CURVE('',#2507,#2512,#1557,.T.);
#3062=EDGE_CURVE('',#2506,#2513,#1558,.T.);
#3063=EDGE_CURVE('',#2505,#2514,#1559,.T.);
#3064=EDGE_CURVE('',#2504,#2515,#1560,.T.);
#3065=EDGE_CURVE('',#2498,#2516,#1561,.T.);
#3066=EDGE_CURVE('',#2516,#2516,#2131,.F.);
#3961=ORIENTED_EDGE('',*,*,#3033,.F.);
#3962=ORIENTED_EDGE('',*,*,#3034,.T.);
#3963=ORIENTED_EDGE('',*,*,#3035,.F.);
#3964=ORIENTED_EDGE('',*,*,#3034,.F.);
#3965=ORIENTED_EDGE('',*,*,#3036,.T.);
#3966=ORIENTED_EDGE('',*,*,#3037,.T.);
#3967=ORIENTED_EDGE('',*,*,#3038,.T.);
#3968=ORIENTED_EDGE('',*,*,#3037,.F.);
#3969=ORIENTED_EDGE('',*,*,#3038,.F.);
#3970=ORIENTED_EDGE('',*,*,#3039,.T.);
#3971=ORIENTED_EDGE('',*,*,#3040,.T.);
#3972=ORIENTED_EDGE('',*,*,#3041,.T.);
#3973=ORIENTED_EDGE('',*,*,#3042,.T.);
#3974=ORIENTED_EDGE('',*,*,#3043,.T.);
#3975=ORIENTED_EDGE('',*,*,#3044,.T.);
#3976=ORIENTED_EDGE('',*,*,#3045,.F.);
#3977=ORIENTED_EDGE('',*,*,#3046,.T.);
#3978=ORIENTED_EDGE('',*,*,#3036,.F.);
#3979=ORIENTED_EDGE('',*,*,#3046,.F.);
#3980=ORIENTED_EDGE('',*,*,#3047,.F.);
#3981=ORIENTED_EDGE('',*,*,#3048,.F.);
#3982=ORIENTED_EDGE('',*,*,#3049,.T.);
#3983=ORIENTED_EDGE('',*,*,#3049,.F.);
#3984=ORIENTED_EDGE('',*,*,#3050,.F.);
#3985=ORIENTED_EDGE('',*,*,#3051,.T.);
#3986=ORIENTED_EDGE('',*,*,#3051,.F.);
#3987=ORIENTED_EDGE('',*,*,#3052,.F.);
#3988=ORIENTED_EDGE('',*,*,#3053,.T.);
#3989=ORIENTED_EDGE('',*,*,#3053,.F.);
#3990=ORIENTED_EDGE('',*,*,#3054,.F.);
#3991=ORIENTED_EDGE('',*,*,#3055,.T.);
#3992=ORIENTED_EDGE('',*,*,#3055,.F.);
#3993=ORIENTED_EDGE('',*,*,#3056,.F.);
#3994=ORIENTED_EDGE('',*,*,#3057,.T.);
#3995=ORIENTED_EDGE('',*,*,#3057,.F.);
#3996=ORIENTED_EDGE('',*,*,#3058,.F.);
#3997=ORIENTED_EDGE('',*,*,#3047,.T.);
#3998=ORIENTED_EDGE('',*,*,#3039,.F.);
#3999=ORIENTED_EDGE('',*,*,#3059,.T.);
#4000=ORIENTED_EDGE('',*,*,#3048,.T.);
#4001=ORIENTED_EDGE('',*,*,#3060,.F.);
#4002=ORIENTED_EDGE('',*,*,#3044,.F.);
#4003=ORIENTED_EDGE('',*,*,#3061,.T.);
#4004=ORIENTED_EDGE('',*,*,#3050,.T.);
#4005=ORIENTED_EDGE('',*,*,#3059,.F.);
#4006=ORIENTED_EDGE('',*,*,#3043,.F.);
#4007=ORIENTED_EDGE('',*,*,#3062,.T.);
#4008=ORIENTED_EDGE('',*,*,#3052,.T.);
#4009=ORIENTED_EDGE('',*,*,#3061,.F.);
#4010=ORIENTED_EDGE('',*,*,#3042,.F.);
#4011=ORIENTED_EDGE('',*,*,#3063,.T.);
#4012=ORIENTED_EDGE('',*,*,#3054,.T.);
#4013=ORIENTED_EDGE('',*,*,#3062,.F.);
#4014=ORIENTED_EDGE('',*,*,#3041,.F.);
#4015=ORIENTED_EDGE('',*,*,#3064,.T.);
#4016=ORIENTED_EDGE('',*,*,#3056,.T.);
#4017=ORIENTED_EDGE('',*,*,#3063,.F.);
#4018=ORIENTED_EDGE('',*,*,#3040,.F.);
#4019=ORIENTED_EDGE('',*,*,#3060,.T.);
#4020=ORIENTED_EDGE('',*,*,#3058,.T.);
#4021=ORIENTED_EDGE('',*,*,#3064,.F.);
#4022=ORIENTED_EDGE('',*,*,#3033,.T.);
#4023=ORIENTED_EDGE('',*,*,#3065,.T.);
#4024=ORIENTED_EDGE('',*,*,#3066,.T.);
#4025=ORIENTED_EDGE('',*,*,#3065,.F.);
#4026=ORIENTED_EDGE('',*,*,#3035,.T.);
#4027=ORIENTED_EDGE('',*,*,#3045,.T.);
#4028=ORIENTED_EDGE('',*,*,#3066,.F.);
#4601=CYLINDRICAL_SURFACE('',#5524,4.99999999999977);
#4602=CYLINDRICAL_SURFACE('',#5538,2.942);
#4816=ADVANCED_FACE('',(#805),#115,.T.);
#4817=ADVANCED_FACE('',(#806),#130,.T.);
#4818=ADVANCED_FACE('',(#807,#412),#545,.T.);
#4819=ADVANCED_FACE('',(#808),#4601,.T.);
#4820=ADVANCED_FACE('',(#809),#546,.F.);
#4821=ADVANCED_FACE('',(#810),#547,.F.);
#4822=ADVANCED_FACE('',(#811),#548,.F.);
#4823=ADVANCED_FACE('',(#812),#549,.F.);
#4824=ADVANCED_FACE('',(#813),#550,.F.);
#4825=ADVANCED_FACE('',(#814),#551,.F.);
#4826=ADVANCED_FACE('',(#815),#552,.F.);
#4827=ADVANCED_FACE('',(#816),#553,.F.);
#4828=ADVANCED_FACE('',(#817),#554,.F.);
#4829=ADVANCED_FACE('',(#818),#555,.F.);
#4830=ADVANCED_FACE('',(#819),#556,.F.);
#4831=ADVANCED_FACE('',(#820),#557,.F.);
#4832=ADVANCED_FACE('',(#821),#4602,.T.);
#4833=ADVANCED_FACE('',(#822),#558,.T.);
#4834=ADVANCED_FACE('',(#823,#413),#559,.T.);
#4996=CLOSED_SHELL('',(#4816,#4817,#4818,#4819,#4820,#4821,#4822,#4823,
#4824,#4825,#4826,#4827,#4828,#4829,#4830,#4831,#4832,#4833,#4834));
#5515=AXIS2_PLACEMENT_3D('',#8522,#6712,#6713);
#5516=AXIS2_PLACEMENT_3D('',#8523,#6714,#6715);
#5517=AXIS2_PLACEMENT_3D('',#8525,#6716,#6717);
#5518=AXIS2_PLACEMENT_3D('',#8528,#6719,#6720);
#5519=AXIS2_PLACEMENT_3D('',#8529,#6721,#6722);
#5520=AXIS2_PLACEMENT_3D('',#8531,#6723,#6724);
#5521=AXIS2_PLACEMENT_3D('',#8533,#6725,#6726);
#5522=AXIS2_PLACEMENT_3D('',#8534,#6727,#6728);
#5523=AXIS2_PLACEMENT_3D('',#8535,#6729,#6730);
#5524=AXIS2_PLACEMENT_3D('',#8548,#6737,#6738);
#5525=AXIS2_PLACEMENT_3D('',#8550,#6739,#6740);
#5526=AXIS2_PLACEMENT_3D('',#8552,#6742,#6743);
#5527=AXIS2_PLACEMENT_3D('',#8559,#6747,#6748);
#5528=AXIS2_PLACEMENT_3D('',#8563,#6751,#6752);
#5529=AXIS2_PLACEMENT_3D('',#8567,#6755,#6756);
#5530=AXIS2_PLACEMENT_3D('',#8571,#6759,#6760);
#5531=AXIS2_PLACEMENT_3D('',#8575,#6763,#6764);
#5532=AXIS2_PLACEMENT_3D('',#8577,#6766,#6767);
#5533=AXIS2_PLACEMENT_3D('',#8580,#6770,#6771);
#5534=AXIS2_PLACEMENT_3D('',#8582,#6773,#6774);
#5535=AXIS2_PLACEMENT_3D('',#8584,#6776,#6777);
#5536=AXIS2_PLACEMENT_3D('',#8586,#6779,#6780);
#5537=AXIS2_PLACEMENT_3D('',#8588,#6782,#6783);
#5538=AXIS2_PLACEMENT_3D('',#8589,#6784,#6785);
#5539=AXIS2_PLACEMENT_3D('',#8592,#6787,#6788);
#5540=AXIS2_PLACEMENT_3D('',#8593,#6789,#6790);
#5541=AXIS2_PLACEMENT_3D('',#8594,#6791,#6792);
#6712=DIRECTION('axis',(0.,0.,1.));
#6713=DIRECTION('refdir',(1.,0.,0.));
#6714=DIRECTION('center_axis',(0.,0.,1.));
#6715=DIRECTION('ref_axis',(-1.,0.,0.));
#6716=DIRECTION('center_axis',(-2.32004514166519E-15,0.,1.));
#6717=DIRECTION('ref_axis',(-1.,0.,-2.32004514166519E-15));
#6718=DIRECTION('',(-0.739271628119017,-9.05346633076407E-17,-0.673407350611988));
#6719=DIRECTION('center_axis',(2.32004514166519E-15,0.,-1.));
#6720=DIRECTION('ref_axis',(-1.,0.,-2.32004514166519E-15));
#6721=DIRECTION('center_axis',(2.32004514166519E-15,0.,-1.));
#6722=DIRECTION('ref_axis',(-1.,0.,-2.30926389122043E-15));
#6723=DIRECTION('center_axis',(-2.32004514166519E-15,0.,1.));
#6724=DIRECTION('ref_axis',(1.,0.,2.32004514166519E-15));
#6725=DIRECTION('center_axis',(-1.22464679914735E-16,-1.,-2.84123585661764E-31));
#6726=DIRECTION('ref_axis',(1.,-1.22464679914735E-16,2.22044604925042E-15));
#6727=DIRECTION('center_axis',(2.32004514166519E-15,0.,-1.));
#6728=DIRECTION('ref_axis',(1.,0.,2.32004514166519E-15));
#6729=DIRECTION('center_axis',(-2.32004514166519E-15,0.,1.));
#6730=DIRECTION('ref_axis',(1.,0.,2.32004514166519E-15));
#6731=DIRECTION('',(-0.866025403784439,-0.5,-2.00921803060872E-15));
#6732=DIRECTION('',(-0.866025403784439,0.5,-2.00921803060872E-15));
#6733=DIRECTION('',(7.69185074553425E-16,1.,1.78454409525905E-30));
#6734=DIRECTION('',(0.866025403784439,0.5,2.00921803060872E-15));
#6735=DIRECTION('',(0.866025403784438,-0.5,2.00921803060872E-15));
#6736=DIRECTION('',(0.,-1.,0.));
#6737=DIRECTION('center_axis',(2.32004514166519E-15,0.,-1.));
#6738=DIRECTION('ref_axis',(-1.,0.,-2.32004514166519E-15));
#6739=DIRECTION('center_axis',(2.32004514166519E-15,0.,-1.));
#6740=DIRECTION('ref_axis',(1.,0.,2.32004514166519E-15));
#6741=DIRECTION('',(-2.32004514166519E-15,0.,1.));
#6742=DIRECTION('center_axis',(0.0435778713738291,-0.0754790873051733,-0.996194698091746));
#6743=DIRECTION('ref_axis',(-0.866025403784439,-0.5,-3.35810244624808E-17));
#6744=DIRECTION('',(1.59381164582915E-16,0.997141949694316,-0.0755508581011305));
#6745=DIRECTION('',(-0.866025403784439,-0.5,0.));
#6746=DIRECTION('',(-0.863550259614423,0.498570974847158,-0.0755508581011305));
#6747=DIRECTION('center_axis',(0.0871557427476581,0.,-0.996194698091746));
#6748=DIRECTION('ref_axis',(0.,-1.,0.));
#6749=DIRECTION('',(0.,-1.,0.));
#6750=DIRECTION('',(-0.863550259614423,-0.498570974847158,-0.0755508581011305));
#6751=DIRECTION('center_axis',(0.0435778713738291,0.0754790873051733,-0.996194698091746));
#6752=DIRECTION('ref_axis',(0.866025403784438,-0.5,-8.05233896096258E-18));
#6753=DIRECTION('',(0.866025403784438,-0.5,0.));
#6754=DIRECTION('',(-1.59381164582915E-16,-0.997141949694316,-0.0755508581011305));
#6755=DIRECTION('center_axis',(-0.0435778713738291,0.0754790873051733,-0.996194698091746));
#6756=DIRECTION('ref_axis',(0.866025403784439,0.5,-3.35810244624808E-17));
#6757=DIRECTION('',(0.866025403784439,0.5,0.));
#6758=DIRECTION('',(0.863550259614423,-0.498570974847159,-0.0755508581011306));
#6759=DIRECTION('center_axis',(-0.0871557427476581,6.70388964831166E-17,
-0.996194698091746));
#6760=DIRECTION('ref_axis',(7.69185074553425E-16,1.,7.59804895741788E-32));
#6761=DIRECTION('',(7.69185074553425E-16,1.,0.));
#6762=DIRECTION('',(0.863550259614423,0.498570974847158,-0.0755508581011305));
#6763=DIRECTION('center_axis',(-0.0435778713738291,-0.0754790873051733,
-0.996194698091746));
#6764=DIRECTION('ref_axis',(-0.866025403784439,0.5,3.35810244624808E-17));
#6765=DIRECTION('',(-0.866025403784439,0.5,0.));
#6766=DIRECTION('center_axis',(0.5,-0.866025403784439,0.));
#6767=DIRECTION('ref_axis',(-0.866025403784439,-0.5,0.));
#6768=DIRECTION('',(0.,0.,-1.));
#6769=DIRECTION('',(0.,0.,-1.));
#6770=DIRECTION('center_axis',(1.,0.,0.));
#6771=DIRECTION('ref_axis',(0.,-1.,0.));
#6772=DIRECTION('',(0.,0.,-1.));
#6773=DIRECTION('center_axis',(0.5,0.866025403784438,0.));
#6774=DIRECTION('ref_axis',(0.866025403784438,-0.5,0.));
#6775=DIRECTION('',(0.,0.,-1.));
#6776=DIRECTION('center_axis',(-0.5,0.866025403784439,0.));
#6777=DIRECTION('ref_axis',(0.866025403784439,0.5,0.));
#6778=DIRECTION('',(0.,0.,-1.));
#6779=DIRECTION('center_axis',(-1.,7.69185074553425E-16,0.));
#6780=DIRECTION('ref_axis',(7.69185074553425E-16,1.,0.));
#6781=DIRECTION('',(0.,0.,-1.));
#6782=DIRECTION('center_axis',(-0.5,-0.866025403784439,0.));
#6783=DIRECTION('ref_axis',(-0.866025403784439,0.5,0.));
#6784=DIRECTION('center_axis',(2.32004514166519E-15,0.,-1.));
#6785=DIRECTION('ref_axis',(-1.,0.,-2.32004514166519E-15));
#6786=DIRECTION('',(-2.32004514166519E-15,0.,1.));
#6787=DIRECTION('center_axis',(-2.32004514166519E-15,0.,1.));
#6788=DIRECTION('ref_axis',(-1.,0.,-2.32004514166519E-15));
#6789=DIRECTION('center_axis',(2.32004514166519E-15,0.,-1.));
#6790=DIRECTION('ref_axis',(-1.,0.,-2.32004514166519E-15));
#6791=DIRECTION('center_axis',(2.32004514166519E-15,0.,-1.));
#6792=DIRECTION('ref_axis',(-1.,0.,-2.32004514166519E-15));
#8522=CARTESIAN_POINT('',(0.,0.,0.));
#8523=CARTESIAN_POINT('Origin',(0.,0.,-15.693275));
#8524=CARTESIAN_POINT('',(2.94200000000002,3.60291088309151E-16,-15.4940369700794));
#8525=CARTESIAN_POINT('Origin',(1.58481671019917E-14,0.,-15.4940369700794));
#8526=CARTESIAN_POINT('',(2.38654999999999,-2.9226808185051E-16,-16.));
#8527=CARTESIAN_POINT('',(2.72327499999996,3.33505001194796E-16,-15.693275));
#8528=CARTESIAN_POINT('Origin',(0.,0.,-16.));
#8529=CARTESIAN_POINT('Origin',(-3.26269418602128E-14,0.,5.39999999999958));
#8530=CARTESIAN_POINT('',(4.99999999999974,-6.12323399573649E-16,5.39999999999959));
#8531=CARTESIAN_POINT('Origin',(-3.26269418602128E-14,0.,5.39999999999958));
#8532=CARTESIAN_POINT('',(4.39999999999974,-5.38844591624807E-16,5.99999999999959));
#8533=CARTESIAN_POINT('Origin',(4.39999999999974,-5.38844591624807E-16,
5.39999999999959));
#8534=CARTESIAN_POINT('Origin',(-3.40189689452119E-14,0.,5.99999999999958));
#8535=CARTESIAN_POINT('Origin',(-4.9999999999998,0.,5.99999999999957));
#8536=CARTESIAN_POINT('',(2.5,-1.44337567297406,6.));
#8537=CARTESIAN_POINT('',(0.,-2.88675134594813,6.));
#8538=CARTESIAN_POINT('',(7.46624984060421E-14,-2.88675134594809,5.99999999999958));
#8539=CARTESIAN_POINT('',(-2.5,-1.44337567297406,6.));
#8540=CARTESIAN_POINT('',(-2.49999999999993,-1.44337567297411,5.99999999999957));
#8541=CARTESIAN_POINT('',(-2.5,1.44337567297407,6.));
#8542=CARTESIAN_POINT('',(-2.5,-0.721687836487033,5.99999999999957));
#8543=CARTESIAN_POINT('',(3.64291929955129E-16,2.88675134594813,6.));
#8544=CARTESIAN_POINT('',(-3.74999999999992,0.721687836487077,5.99999999999957));
#8545=CARTESIAN_POINT('',(2.5,1.44337567297406,6.));
#8546=CARTESIAN_POINT('',(-1.24999999999992,3.60843918243512,5.99999999999958));
#8547=CARTESIAN_POINT('',(2.5,0.721687836487032,5.99999999999958));
#8548=CARTESIAN_POINT('Origin',(-2.70588335202164E-14,0.,2.99999999999958));
#8549=CARTESIAN_POINT('',(4.99999999999975,-6.12323399573649E-16,-4.10227407598995E-13));
#8550=CARTESIAN_POINT('Origin',(-2.00986980952208E-14,0.,-4.2159796951126E-13));
#8551=CARTESIAN_POINT('',(4.99999999999974,-6.12323399573649E-16,2.99999999999959));
#8552=CARTESIAN_POINT('Origin',(0.,-2.88675134594813,3.));
#8553=CARTESIAN_POINT('',(0.,-2.88675134594813,3.));
#8554=CARTESIAN_POINT('',(-1.31861671037658E-15,-5.55111512312578E-16,2.78127834118519));
#8555=CARTESIAN_POINT('',(-1.66533453693773E-15,-2.16918285467233,2.9456316973939));
#8556=CARTESIAN_POINT('',(2.5,-1.44337567297406,3.));
#8557=CARTESIAN_POINT('',(1.24247637239728E-16,-2.88675134594813,3.));
#8558=CARTESIAN_POINT('',(1.87856745759988,-1.08459142733617,2.9456316973939));
#8559=CARTESIAN_POINT('Origin',(2.5,-1.44337567297406,3.));
#8560=CARTESIAN_POINT('',(2.5,1.44337567297406,3.));
#8561=CARTESIAN_POINT('',(2.5,-1.44337567297406,3.));
#8562=CARTESIAN_POINT('',(1.87856745759989,1.08459142733616,2.9456316973939));
#8563=CARTESIAN_POINT('Origin',(2.5,1.44337567297406,3.));
#8564=CARTESIAN_POINT('',(5.55111512312578E-16,2.88675134594813,3.));
#8565=CARTESIAN_POINT('',(2.5,1.44337567297406,3.));
#8566=CARTESIAN_POINT('',(1.38777878078145E-15,2.16918285467233,2.9456316973939));
#8567=CARTESIAN_POINT('Origin',(5.55111512312578E-16,2.88675134594813,3.));
#8568=CARTESIAN_POINT('',(-2.5,1.44337567297407,3.));
#8569=CARTESIAN_POINT('',(3.64291929955129E-16,2.88675134594813,3.));
#8570=CARTESIAN_POINT('',(-1.87856745759989,1.08459142733617,2.9456316973939));
#8571=CARTESIAN_POINT('Origin',(-2.5,1.44337567297407,3.));
#8572=CARTESIAN_POINT('',(-2.5,-1.44337567297406,3.));
#8573=CARTESIAN_POINT('',(-2.5,1.44337567297407,3.));
#8574=CARTESIAN_POINT('',(-1.87856745759989,-1.08459142733616,2.9456316973939));
#8575=CARTESIAN_POINT('Origin',(-2.5,-1.44337567297406,3.));
#8576=CARTESIAN_POINT('',(-2.5,-1.44337567297406,3.));
#8577=CARTESIAN_POINT('Origin',(2.5,-1.44337567297406,6.));
#8578=CARTESIAN_POINT('',(2.5,-1.44337567297406,6.));
#8579=CARTESIAN_POINT('',(0.,-2.88675134594813,6.));
#8580=CARTESIAN_POINT('Origin',(2.5,1.44337567297406,6.));
#8581=CARTESIAN_POINT('',(2.5,1.44337567297406,6.));
#8582=CARTESIAN_POINT('Origin',(0.,2.88675134594813,6.));
#8583=CARTESIAN_POINT('',(3.64291929955129E-16,2.88675134594813,6.));
#8584=CARTESIAN_POINT('Origin',(-2.5,1.44337567297407,6.));
#8585=CARTESIAN_POINT('',(-2.5,1.44337567297407,6.));
#8586=CARTESIAN_POINT('Origin',(-2.5,-1.44337567297406,6.));
#8587=CARTESIAN_POINT('',(-2.5,-1.44337567297406,6.));
#8588=CARTESIAN_POINT('Origin',(0.,-2.88675134594813,6.));
#8589=CARTESIAN_POINT('Origin',(-1.53833696190003E-15,0.,-8.00000000000013));
#8590=CARTESIAN_POINT('',(2.94199999999998,3.60291088309151E-16,-2.53037902429339E-13));
#8591=CARTESIAN_POINT('',(2.942,-3.60291088309151E-16,-8.00000000000012));
#8592=CARTESIAN_POINT('Origin',(-2.00986980952212E-14,0.,-2.59792187762287E-13));
#8593=CARTESIAN_POINT('Origin',(1.72084568816899E-14,0.,-16.));
#8594=CARTESIAN_POINT('Origin',(-2.9999999999998,0.,-2.66583504750515E-13));
#9479=UNCERTAINTY_MEASURE_WITH_UNIT(LENGTH_MEASURE(0.01),#9497,
'DISTANCE_ACCURACY_VALUE',
'Maximum model space distance between geometric entities at asserted c
onnectivities');
#9485=UNCERTAINTY_MEASURE_WITH_UNIT(LENGTH_MEASURE(0.01),#9497,
'DISTANCE_ACCURACY_VALUE',
'Maximum model space distance between geometric entities at asserted c
onnectivities');
#9490=(
GEOMETRIC_REPRESENTATION_CONTEXT(3)
GLOBAL_UNCERTAINTY_ASSIGNED_CONTEXT((#9479))
GLOBAL_UNIT_ASSIGNED_CONTEXT((#9497,#9499,#9500))
REPRESENTATION_CONTEXT('','3D')
);
#9496=(
GEOMETRIC_REPRESENTATION_CONTEXT(3)
GLOBAL_UNCERTAINTY_ASSIGNED_CONTEXT((#9485))
GLOBAL_UNIT_ASSIGNED_CONTEXT((#9497,#9499,#9500))
REPRESENTATION_CONTEXT('','3D')
);
#9497=(
LENGTH_UNIT()
NAMED_UNIT(*)
SI_UNIT(.MILLI.,.METRE.)
);
#9499=(
NAMED_UNIT(*)
PLANE_ANGLE_UNIT()
SI_UNIT($,.RADIAN.)
);
#9500=(
NAMED_UNIT(*)
SI_UNIT($,.STERADIAN.)
SOLID_ANGLE_UNIT()
);
#9505=SHAPE_DEFINITION_REPRESENTATION(#9515,#9542);
#9515=PRODUCT_DEFINITION_SHAPE('',$,#9553);
#9542=SHAPE_REPRESENTATION('',(#5515),#9490);
#9548=PRODUCT_DEFINITION_CONTEXT('part definition',#9580,'design');
#9553=PRODUCT_DEFINITION(
'Broached Hexagon Socket Head Cap Screw ASME B18.3.1M - M6x1 x 16 Stee
l Grade 2 Plain v1',
'Broached Hexagon Socket Head Cap Screw ASME B18.3.1M - M6x1 x 16 Stee
l Grade 2 Plain v1',#9563,#9548);
#9563=PRODUCT_DEFINITION_FORMATION('',$,#9586);
#9580=APPLICATION_CONTEXT(
'Core Data for Automotive Mechanical Design Process');
#9581=PRODUCT_CONTEXT('part definition',#9580,'mechanical');
#9586=PRODUCT(
'Broached Hexagon Socket Head Cap Screw ASME B18.3.1M - M6x1 x 16 Stee
l Grade 2 Plain v1',
'Broached Hexagon Socket Head Cap Screw ASME B18.3.1M - M6x1 x 16 Stee
l Grade 2 Plain v1',
'Broached Hexagon Socket Head Cap Screw ASME B18.3.1M - M6x1 x 16',(#9581));
#9594=PRESENTATION_STYLE_ASSIGNMENT((#9597));
#9597=SURFACE_STYLE_USAGE(.BOTH.,#9600);
#9600=SURFACE_SIDE_STYLE('',(#9603));
#9603=SURFACE_STYLE_FILL_AREA(#9606);
#9606=FILL_AREA_STYLE('Opaque(160,160,160)',(#9609));
#9609=FILL_AREA_STYLE_COLOUR('Opaque(160,160,160)',#9612);
#9612=COLOUR_RGB('Opaque(160,160,160)', 0.40784314, 0.44705882, 0.49803922);
ENDSEC;
END-ISO-10303-21;
